ISO-10303-21;
HEADER;
FILE_DESCRIPTION (('STEP AP203'),
    '1' );
FILE_NAME ('bench vise8-.step',
    '2026-10-07T23:37:23',
    ( '' ),
    ( '' ),
    'SwSTEP 2.0',
    'SolidWorks 2024',
    '' );
FILE_SCHEMA (( 'AUTOMOTIVE_DESIGN' ));
ENDSEC;

DATA;
#64=AXIS2_PLACEMENT_3D ( 'NONE', #1983, #3374, #5790 ) ;
#71=FACE_OUTER_BOUND ( 'NONE', #866, .T. ) ;
#73=CIRCLE ( 'NONE', #872, 1.124999999999999556 ) ;
#173=AXIS2_PLACEMENT_3D ( 'NONE', #3203, #1935, #2062 ) ;
#310=DIRECTION ( 'NONE',  ( 0.000000000000000000, 0.000000000000000000, 1.000000000000000000 ) ) ;
#464=CARTESIAN_POINT ( 'NONE',  ( 0.000000000000000000, 3.950000000000000178, 7.131250000000001421 ) ) ;
#515=ADVANCED_FACE ( 'NONE', ( #3815 ), #876, .T. ) ;
#534=CARTESIAN_POINT ( 'NONE',  ( -1.124999999999999556, 3.950000000000000178, 6.956250000000000711 ) ) ;
#606=CIRCLE ( 'NONE', #1393, 1.124999999999999556 ) ;
#607=MECHANICAL_CONTEXT ( 'NONE', #3567, 'mechanical' ) ;
#670=EDGE_CURVE ( 'NONE', #1901, #3103, #606, .T. ) ;
#671=ORIENTED_EDGE ( 'NONE', *, *, #7837, .T. ) ;
#738=FACE_OUTER_BOUND ( 'NONE', #8163, .T. ) ;
#866=EDGE_LOOP ( 'NONE', ( #2004, #3367, #671, #6711 ) ) ;
#872=AXIS2_PLACEMENT_3D ( 'NONE', #4937, #1827, #4319 ) ;
#876=PLANE ( 'NONE',  #64 ) ;
#927=LINE ( 'NONE', #5920, #3990 ) ;
#1097=CIRCLE ( 'NONE', #5667, 1.124999999999999556 ) ;
#1348=( NAMED_UNIT ( * ) PLANE_ANGLE_UNIT ( ) SI_UNIT ( $, .RADIAN. ) );
#1393=AXIS2_PLACEMENT_3D ( 'NONE', #464, #5911, #5409 ) ;
#1500=VERTEX_POINT ( 'NONE', #534 ) ;
#1513=( GEOMETRIC_REPRESENTATION_CONTEXT ( 3 ) GLOBAL_UNCERTAINTY_ASSIGNED_CONTEXT ( ( #1612 ) ) GLOBAL_UNIT_ASSIGNED_CONTEXT ( ( #4457, #1348, #3838 ) ) REPRESENTATION_CONTEXT ( 'NONE', 'WORKASPACE' ) );
#1536=ADVANCED_FACE ( 'NONE', ( #71 ), #8094, .T. ) ;
#1612=UNCERTAINTY_MEASURE_WITH_UNIT (LENGTH_MEASURE( 1.000000000000000082E-05 ), #4457, 'distance_accuracy_value', 'NONE');
#1624=ORIENTED_EDGE ( 'NONE', *, *, #7047, .F. ) ;
#1662=EDGE_CURVE ( 'NONE', #1500, #3103, #2093, .T. ) ;
#1742=VERTEX_POINT ( 'NONE', #2467 ) ;
#1827=DIRECTION ( 'NONE',  ( -0.000000000000000000, -0.000000000000000000, -1.000000000000000000 ) ) ;
#1846=MANIFOLD_SOLID_BREP ( 'Imported1', #2029 ) ;
#1901=VERTEX_POINT ( 'NONE', #5685 ) ;
#1904=EDGE_LOOP ( 'NONE', ( #5706, #4163 ) ) ;
#1925=LENGTH_MEASURE_WITH_UNIT ( LENGTH_MEASURE( 0.02539999999999999897 ), #8177 );
#1935=DIRECTION ( 'NONE',  ( -0.000000000000000000, -0.000000000000000000, -1.000000000000000000 ) ) ;
#1983=CARTESIAN_POINT ( 'NONE',  ( 1.124999999999999556, 3.950000000000000178, 6.956250000000000711 ) ) ;
#2001=CARTESIAN_POINT ( 'NONE',  ( -1.124999999999999556, 3.950000000000000178, 6.956250000000000711 ) ) ;
#2004=ORIENTED_EDGE ( 'NONE', *, *, #5623, .F. ) ;
#2029=CLOSED_SHELL ( 'NONE', ( #1536, #515, #2695, #4882 ) ) ;
#2062=DIRECTION ( 'NONE',  ( 1.000000000000000000, 0.000000000000000000, 0.000000000000000000 ) ) ;
#2093=LINE ( 'NONE', #2001, #4392 ) ;
#2146=CIRCLE ( 'NONE', #173, 1.124999999999999556 ) ;
#2226=DIRECTION ( 'NONE',  ( -0.000000000000000000, -0.000000000000000000, -1.000000000000000000 ) ) ;
#2257=DESIGN_CONTEXT ( 'detailed design', #8182, 'design' ) ;
#2326=DIRECTION ( 'NONE',  ( 1.000000000000000000, 0.000000000000000000, 0.000000000000000000 ) ) ;
#2467=CARTESIAN_POINT ( 'NONE',  ( 1.124999999999999556, 3.950000000000000178, 6.956250000000000711 ) ) ;
#2621=PLANE ( 'NONE',  #6073 ) ;
#2672=PRODUCT_DEFINITION_SHAPE ( 'NONE', 'NONE',  #4922 ) ;
#2695=ADVANCED_FACE ( 'NONE', ( #4192 ), #6676, .T. ) ;
#3103=VERTEX_POINT ( 'NONE', #4684 ) ;
#3203=CARTESIAN_POINT ( 'NONE',  ( 0.000000000000000000, 3.950000000000000178, 6.956250000000000711 ) ) ;
#3367=ORIENTED_EDGE ( 'NONE', *, *, #1662, .T. ) ;
#3374=DIRECTION ( 'NONE',  ( 0.000000000000000000, 0.000000000000000000, -1.000000000000000000 ) ) ;
#3567=APPLICATION_CONTEXT ( 'configuration controlled 3d designs of mechanical parts and assemblies' ) ;
#3692=DIRECTION ( 'NONE',  ( 0.000000000000000000, 0.000000000000000000, 1.000000000000000000 ) ) ;
#3730=CARTESIAN_POINT ( 'NONE',  ( 0.000000000000000000, 3.950000000000000178, 6.956250000000000711 ) ) ;
#3733=ORIENTED_EDGE ( 'NONE', *, *, #670, .F. ) ;
#3736=CARTESIAN_POINT ( 'NONE',  ( 0.000000000000000000, 0.000000000000000000, 0.000000000000000000 ) ) ;
#3751=AXIS2_PLACEMENT_3D ( 'NONE', #5424, #7986, #2326 ) ;
#3806=DIMENSIONAL_EXPONENTS ( 1.000000000000000000, 0.000000000000000000, 0.000000000000000000, 0.000000000000000000, 0.000000000000000000, 0.000000000000000000, 0.000000000000000000 ) ;
#3815=FACE_OUTER_BOUND ( 'NONE', #1904, .T. ) ;
#3838=( NAMED_UNIT ( * ) SI_UNIT ( $, .STERADIAN. ) SOLID_ANGLE_UNIT ( ) );
#3990=VECTOR ( 'NONE', #310, 39.37007874015748143 ) ;
#4163=ORIENTED_EDGE ( 'NONE', *, *, #5623, .T. ) ;
#4192=FACE_OUTER_BOUND ( 'NONE', #7708, .T. ) ;
#4319=DIRECTION ( 'NONE',  ( 1.000000000000000000, 0.000000000000000000, 0.000000000000000000 ) ) ;
#4347=PRODUCT_DEFINITION_FORMATION_WITH_SPECIFIED_SOURCE ( 'ANY', '', #8109, .NOT_KNOWN. ) ;
#4392=VECTOR ( 'NONE', #6964, 39.37007874015748143 ) ;
#4429=ORIENTED_EDGE ( 'NONE', *, *, #7837, .F. ) ;
#4457=( CONVERSION_BASED_UNIT ( 'INCH', #1925 ) LENGTH_UNIT ( ) NAMED_UNIT ( #3806 ) );
#4496=CARTESIAN_POINT ( 'NONE',  ( 0.000000000000000000, 3.950000000000000178, 7.131250000000001421 ) ) ;
#4684=CARTESIAN_POINT ( 'NONE',  ( -1.124999999999999556, 3.950000000000000178, 7.131250000000001421 ) ) ;
#4882=ADVANCED_FACE ( 'N', ( #738 ), #2621, .T. ) ;
#4922=PRODUCT_DEFINITION ( 'UNKNOWN', '', #4347, #2257 ) ;
#4937=CARTESIAN_POINT ( 'NONE',  ( 0.000000000000000000, 3.950000000000000178, 6.956250000000000711 ) ) ;
#5111=DIRECTION ( 'NONE',  ( 0.000000000000000000, 0.000000000000000000, 1.000000000000000000 ) ) ;
#5409=DIRECTION ( 'NONE',  ( 1.000000000000000000, 0.000000000000000000, 0.000000000000000000 ) ) ;
#5424=CARTESIAN_POINT ( 'NONE',  ( 0.000000000000000000, 3.950000000000000178, 6.956250000000000711 ) ) ;
#5458=ADVANCED_BREP_SHAPE_REPRESENTATION ( '', ( #1846, #7272 ), #1513 ) ;
#5618=DIRECTION ( 'NONE',  ( 1.000000000000000000, 0.000000000000000000, 0.000000000000000000 ) ) ;
#5623=EDGE_CURVE ( 'NONE', #1500, #1742, #2146, .T. ) ;
#5648=DIRECTION ( 'NONE',  ( 1.000000000000000000, 0.000000000000000000, 0.000000000000000000 ) ) ;
#5667=AXIS2_PLACEMENT_3D ( 'NONE', #5954, #2226, #7887 ) ;
#5685=CARTESIAN_POINT ( 'NONE',  ( 1.124999999999999556, 3.950000000000000178, 7.131250000000001421 ) ) ;
#5706=ORIENTED_EDGE ( 'NONE', *, *, #7047, .T. ) ;
#5790=DIRECTION ( 'NONE',  ( -1.000000000000000000, 0.000000000000000000, -0.000000000000000000 ) ) ;
#5799=SHAPE_DEFINITION_REPRESENTATION ( #2672, #6925 ) ;
#5911=DIRECTION ( 'NONE',  ( -0.000000000000000000, -0.000000000000000000, -1.000000000000000000 ) ) ;
#5920=CARTESIAN_POINT ( 'NONE',  ( 1.124999999999999556, 3.950000000000000178, 6.956250000000000711 ) ) ;
#5954=CARTESIAN_POINT ( 'NONE',  ( 0.000000000000000000, 3.950000000000000178, 7.131250000000001421 ) ) ;
#6073=AXIS2_PLACEMENT_3D ( 'NONE', #4496, #5111, #7650 ) ;
#6237=DIRECTION ( 'NONE',  ( 0.000000000000000000, 0.000000000000000000, 1.000000000000000000 ) ) ;
#6247=AXIS2_PLACEMENT_3D ( 'NONE', #3730, #3692, #5648 ) ;
#6280=ORIENTED_EDGE ( 'NONE', *, *, #6896, .T. ) ;
#6354=SHAPE_REPRESENTATION_RELATIONSHIP ( 'NONE' , 'NONE' ,  #6925, #5458 ) ;
#6434=ORIENTED_EDGE ( 'NONE', *, *, #1662, .F. ) ;
#6676=CYLINDRICAL_SURFACE ( 'NONE', #3751, 1.124999999999999556 ) ;
#6711=ORIENTED_EDGE ( 'NONE', *, *, #6896, .F. ) ;
#6896=EDGE_CURVE ( 'NONE', #1742, #1901, #927, .T. ) ;
#6925=SHAPE_REPRESENTATION ( 'bench vise8-', ( #7272 ), #1513 ) ;
#6964=DIRECTION ( 'NONE',  ( 0.000000000000000000, 0.000000000000000000, 1.000000000000000000 ) ) ;
#7047=EDGE_CURVE ( 'NONE', #1742, #1500, #73, .T. ) ;
#7272=AXIS2_PLACEMENT_3D ( 'NONE', #3736, #6237, #5618 ) ;
#7650=DIRECTION ( 'NONE',  ( 1.000000000000000000, 0.000000000000000000, -0.000000000000000000 ) ) ;
#7708=EDGE_LOOP ( 'NONE', ( #6434, #1624, #6280, #7732 ) ) ;
#7732=ORIENTED_EDGE ( 'NONE', *, *, #670, .T. ) ;
#7837=EDGE_CURVE ( 'NONE', #3103, #1901, #1097, .T. ) ;
#7887=DIRECTION ( 'NONE',  ( 1.000000000000000000, 0.000000000000000000, 0.000000000000000000 ) ) ;
#7986=DIRECTION ( 'NONE',  ( 0.000000000000000000, 0.000000000000000000, 1.000000000000000000 ) ) ;
#8094=CYLINDRICAL_SURFACE ( 'NONE', #6247, 1.124999999999999556 ) ;
#8109=PRODUCT ( 'bench vise8-', 'bench vise8-', '', ( #607 ) ) ;
#8163=EDGE_LOOP ( 'NONE', ( #3733, #4429 ) ) ;
#8177=( LENGTH_UNIT ( ) NAMED_UNIT ( * ) SI_UNIT ( $, .METRE. ) );
#8182=APPLICATION_CONTEXT ( 'configuration controlled 3d designs of mechanical parts and assemblies' ) ;
#8206=COLOUR_RGB('Light Blue', 0.31764706, 0.68627451, 0.89019608);
#8207=FILL_AREA_STYLE_COLOUR('',#8206);
#8208=FILL_AREA_STYLE('',(#8207));
#8209=SURFACE_STYLE_FILL_AREA(#8208);
#8210=SURFACE_SIDE_STYLE('',(#8209));
#8211=SURFACE_STYLE_USAGE(.BOTH.,#8210);
#8212=PRESENTATION_STYLE_ASSIGNMENT((#8211));
#8255=STYLED_ITEM('',(#8212),#1846);
#8256=MECHANICAL_DESIGN_GEOMETRIC_PRESENTATION_REPRESENTATION('',(#8255),#1513);
ENDSEC;
END-ISO-10303-21;
